ISO-10303-21;
HEADER;
/* Generated by software containing ST-Developer
 * from STEP Tools, Inc. (www.steptools.com) 
 */

FILE_DESCRIPTION(
/* description */ ('Belt tension measurement rig'),
/* implementation_level */ '2;1');

FILE_NAME(
/* name */ 'Output M3 set screw.step',
/* time_stamp */ '2026-10-28T03:24:44-07:00',
/* author */ (''),
/* organization */ (''),
/* preprocessor_version */ 'ST-DEVELOPER v20.2',
/* originating_system */ 'Autodesk Translation Framework v15.17.0.0',
/* authorisation */ '');

FILE_SCHEMA (('AUTOMOTIVE_DESIGN { 1 0 10303 214 3 1 1 }'));
ENDSEC;

DATA;
#10=MECHANICAL_DESIGN_GEOMETRIC_PRESENTATION_REPRESENTATION('',(#754),#23587);
#629=SHAPE_REPRESENTATION_RELATIONSHIP('SRR','None',#23880,#684);
#684=ADVANCED_BREP_SHAPE_REPRESENTATION('',(#822),#23578);
#754=STYLED_ITEM('',(#24218),#822);
#822=MANIFOLD_SOLID_BREP('Body1',#12261);
#1308=PLANE('',#14054);
#1309=PLANE('',#14055);
#1900=FACE_OUTER_BOUND('',#2788,.T.);
#1901=FACE_OUTER_BOUND('',#2789,.T.);
#1902=FACE_OUTER_BOUND('',#2790,.T.);
#2788=EDGE_LOOP('',(#10372,#10373,#10374,#10375));
#2789=EDGE_LOOP('',(#10376));
#2790=EDGE_LOOP('',(#10377));
#3565=LINE('',#22217,#4316);
#4316=VECTOR('',#17468,0.15);
#5028=CIRCLE('',#14052,0.15);
#5029=CIRCLE('',#14053,0.15);
#6065=VERTEX_POINT('',#22214);
#6066=VERTEX_POINT('',#22216);
#7545=EDGE_CURVE('',#6065,#6065,#5028,.T.);
#7546=EDGE_CURVE('',#6065,#6066,#3565,.T.);
#7547=EDGE_CURVE('',#6066,#6066,#5029,.T.);
#10372=ORIENTED_EDGE('',*,*,#7545,.F.);
#10373=ORIENTED_EDGE('',*,*,#7546,.T.);
#10374=ORIENTED_EDGE('',*,*,#7547,.T.);
#10375=ORIENTED_EDGE('',*,*,#7546,.F.);
#10376=ORIENTED_EDGE('',*,*,#7545,.T.);
#10377=ORIENTED_EDGE('',*,*,#7547,.F.);
#11387=CYLINDRICAL_SURFACE('',#14051,0.15);
#12041=ADVANCED_FACE('',(#1900),#11387,.T.);
#12042=ADVANCED_FACE('',(#1901),#1308,.T.);
#12043=ADVANCED_FACE('',(#1902),#1309,.F.);
#12261=CLOSED_SHELL('',(#12041,#12042,#12043));
#14050=AXIS2_PLACEMENT_3D('',#22212,#17462,#17463);
#14051=AXIS2_PLACEMENT_3D('',#22213,#17464,#17465);
#14052=AXIS2_PLACEMENT_3D('',#22215,#17466,#17467);
#14053=AXIS2_PLACEMENT_3D('',#22218,#17469,#17470);
#14054=AXIS2_PLACEMENT_3D('',#22219,#17471,#17472);
#14055=AXIS2_PLACEMENT_3D('',#22220,#17473,#17474);
#17462=DIRECTION('axis',(0.,0.,1.));
#17463=DIRECTION('refdir',(1.,0.,0.));
#17464=DIRECTION('center_axis',(0.,0.,1.));
#17465=DIRECTION('ref_axis',(1.,0.,0.));
#17466=DIRECTION('center_axis',(0.,0.,1.));
#17467=DIRECTION('ref_axis',(1.,0.,0.));
#17468=DIRECTION('',(0.,0.,-1.));
#17469=DIRECTION('center_axis',(0.,0.,1.));
#17470=DIRECTION('ref_axis',(1.,0.,0.));
#17471=DIRECTION('center_axis',(0.,0.,1.));
#17472=DIRECTION('ref_axis',(1.,0.,0.));
#17473=DIRECTION('center_axis',(0.,0.,1.));
#17474=DIRECTION('ref_axis',(1.,0.,0.));
#22212=CARTESIAN_POINT('',(0.,0.,0.));
#22213=CARTESIAN_POINT('Origin',(10.,-4.,6.));
#22214=CARTESIAN_POINT('',(9.85,-4.,6.4));
#22215=CARTESIAN_POINT('Origin',(10.,-4.,6.4));
#22216=CARTESIAN_POINT('',(9.85,-4.,6.));
#22217=CARTESIAN_POINT('',(9.85,-4.,6.));
#22218=CARTESIAN_POINT('Origin',(10.,-4.,6.));
#22219=CARTESIAN_POINT('Origin',(10.,-4.,6.4));
#22220=CARTESIAN_POINT('Origin',(10.,-4.,6.));
#23513=UNCERTAINTY_MEASURE_WITH_UNIT(LENGTH_MEASURE(0.001),#23588,
'DISTANCE_ACCURACY_VALUE',
'Maximum model space distance between geometric entities at asserted c
onnectivities');
#23522=UNCERTAINTY_MEASURE_WITH_UNIT(LENGTH_MEASURE(0.001),#23588,
'DISTANCE_ACCURACY_VALUE',
'Maximum model space distance between geometric entities at asserted c
onnectivities');
#23578=(
GEOMETRIC_REPRESENTATION_CONTEXT(3)
GLOBAL_UNCERTAINTY_ASSIGNED_CONTEXT((#23513))
GLOBAL_UNIT_ASSIGNED_CONTEXT((#23588,#23590,#23591))
REPRESENTATION_CONTEXT('','3D')
);
#23587=(
GEOMETRIC_REPRESENTATION_CONTEXT(3)
GLOBAL_UNCERTAINTY_ASSIGNED_CONTEXT((#23522))
GLOBAL_UNIT_ASSIGNED_CONTEXT((#23588,#23590,#23591))
REPRESENTATION_CONTEXT('','3D')
);
#23588=(
LENGTH_UNIT()
NAMED_UNIT(*)
SI_UNIT(.CENTI.,.METRE.)
);
#23590=(
NAMED_UNIT(*)
PLANE_ANGLE_UNIT()
SI_UNIT($,.RADIAN.)
);
#23591=(
NAMED_UNIT(*)
SI_UNIT($,.STERADIAN.)
SOLID_ANGLE_UNIT()
);
#23647=SHAPE_DEFINITION_REPRESENTATION(#23724,#23880);
#23724=PRODUCT_DEFINITION_SHAPE('',$,#23945);
#23880=SHAPE_REPRESENTATION('',(#14050),#23578);
#23889=PRODUCT_DEFINITION_CONTEXT('part definition',#24083,'design');
#23945=PRODUCT_DEFINITION('Output M3 set screw','Output M3 set screw',#24009,
#23889);
#24009=PRODUCT_DEFINITION_FORMATION('',$,#24140);
#24083=APPLICATION_CONTEXT(
'Core Data for Automotive Mechanical Design Process');
#24084=PRODUCT_CONTEXT('part definition',#24083,'mechanical');
#24140=PRODUCT('Output M3 set screw','Output M3 set screw',
'Output M3 set screw',(#24084));
#24212=COLOUR_RGB('Black',0.12,0.14,0.17);
#24213=FILL_AREA_STYLE_COLOUR('',#24212);
#24214=FILL_AREA_STYLE('',(#24213));
#24215=SURFACE_STYLE_FILL_AREA(#24214);
#24216=SURFACE_SIDE_STYLE('',(#24215));
#24217=SURFACE_STYLE_USAGE(.BOTH.,#24216);
#24218=PRESENTATION_STYLE_ASSIGNMENT((#24217));
ENDSEC;
END-ISO-10303-21;
